ISO-10303-21;
HEADER;
FILE_DESCRIPTION((''),'2;1');
FILE_NAME('LEVER_PIVOT_NUT_M10.step','2026-10-01T22:06:14-07:00',(''),(''),'','','');
FILE_SCHEMA (('AUTOMOTIVE_DESIGN { 1 0 10303 214 3 1 1 }'));
ENDSEC;
DATA;
#10=MECHANICAL_DESIGN_GEOMETRIC_PRESENTATION_REPRESENTATION('',(#1033),#50440);
#932=SHAPE_REPRESENTATION_RELATIONSHIP('SRR','None',#50667,#977) ;
#977=ADVANCED_BREP_SHAPE_REPRESENTATION('',(#1086),#50436) ;
#1033=STYLED_ITEM('',(#50883),#1086) ;
#1086=MANIFOLD_SOLID_BREP('LEVER_PIVOT_NUT_M10',#28711) ;
#1404=FACE_BOUND('',#5698,.T.) ;
#1405=FACE_BOUND('',#5704,.T.) ;
#2323=PLANE('',#32249) ;
#2324=PLANE('',#32250) ;
#2325=PLANE('',#32251) ;
#2326=PLANE('',#32252) ;
#2327=PLANE('',#32253) ;
#2328=PLANE('',#32254) ;
#2329=PLANE('',#32255) ;
#2330=PLANE('',#32256) ;
#3848=FACE_OUTER_BOUND('',#5694,.T.) ;
#3849=FACE_OUTER_BOUND('',#5695,.T.) ;
#3850=FACE_OUTER_BOUND('',#5696,.T.) ;
#3851=FACE_OUTER_BOUND('',#5697,.T.) ;
#3852=FACE_OUTER_BOUND('',#5699,.T.) ;
#3853=FACE_OUTER_BOUND('',#5700,.T.) ;
#3854=FACE_OUTER_BOUND('',#5701,.T.) ;
#3855=FACE_OUTER_BOUND('',#5702,.T.) ;
#3856=FACE_OUTER_BOUND('',#5703,.T.) ;
#5694=EDGE_LOOP('',(#26433,#26434,#26435,#26436)) ;
#5695=EDGE_LOOP('',(#26437,#26438,#26439,#26440)) ;
#5696=EDGE_LOOP('',(#26441,#26442,#26443,#26444)) ;
#5697=EDGE_LOOP('',(#26445,#26446,#26447,#26448,#26449,#26450)) ;
#5698=EDGE_LOOP('',(#26451)) ;
#5699=EDGE_LOOP('',(#26452,#26453,#26454,#26455)) ;
#5700=EDGE_LOOP('',(#26456,#26457,#26458,#26459)) ;
#5701=EDGE_LOOP('',(#26460,#26461,#26462,#26463)) ;
#5702=EDGE_LOOP('',(#26464,#26465,#26466,#26467)) ;
#5703=EDGE_LOOP('',(#26468,#26469,#26470,#26471,#26472,#26473)) ;
#5704=EDGE_LOOP('',(#26474)) ;
#8180=LINE('',#50041,#10652) ;
#8181=LINE('',#50046,#10653) ;
#8182=LINE('',#50048,#10654) ;
#8183=LINE('',#50050,#10655) ;
#8184=LINE('',#50051,#10656) ;
#8185=LINE('',#50055,#10657) ;
#8186=LINE('',#50057,#10658) ;
#8187=LINE('',#50059,#10659) ;
#8188=LINE('',#50060,#10660) ;
#8189=LINE('',#50063,#10661) ;
#8190=LINE('',#50064,#10662) ;
#8191=LINE('',#50066,#10663) ;
#8192=LINE('',#50067,#10664) ;
#8193=LINE('',#50070,#10665) ;
#8194=LINE('',#50071,#10666) ;
#8195=LINE('',#50074,#10667) ;
#8196=LINE('',#50075,#10668) ;
#8197=LINE('',#50077,#10669) ;
#8198=LINE('',#50079,#10670) ;
#10652=VECTOR('',#40901,0.5) ;
#10653=VECTOR('',#40906,1.) ;
#10654=VECTOR('',#40907,1.) ;
#10655=VECTOR('',#40908,1.) ;
#10656=VECTOR('',#40909,1.) ;
#10657=VECTOR('',#40912,1.) ;
#10658=VECTOR('',#40913,1.) ;
#10659=VECTOR('',#40914,1.) ;
#10660=VECTOR('',#40915,1.) ;
#10661=VECTOR('',#40918,1.) ;
#10662=VECTOR('',#40919,1.) ;
#10663=VECTOR('',#40920,1.) ;
#10664=VECTOR('',#40921,1.) ;
#10665=VECTOR('',#40924,1.) ;
#10666=VECTOR('',#40925,1.) ;
#10667=VECTOR('',#40928,1.) ;
#10668=VECTOR('',#40929,1.) ;
#10669=VECTOR('',#40932,1.) ;
#10670=VECTOR('',#40935,1.) ;
#11808=CIRCLE('',#32247,0.5) ;
#11809=CIRCLE('',#32248,0.5) ;
#14490=VERTEX_POINT('',#50038) ;
#14491=VERTEX_POINT('',#50040) ;
#14492=VERTEX_POINT('',#50044) ;
#14493=VERTEX_POINT('',#50045) ;
#14494=VERTEX_POINT('',#50047) ;
#14495=VERTEX_POINT('',#50049) ;
#14496=VERTEX_POINT('',#50053) ;
#14497=VERTEX_POINT('',#50054) ;
#14498=VERTEX_POINT('',#50056) ;
#14499=VERTEX_POINT('',#50058) ;
#14500=VERTEX_POINT('',#50062) ;
#14501=VERTEX_POINT('',#50065) ;
#14502=VERTEX_POINT('',#50069) ;
#14503=VERTEX_POINT('',#50073) ;
#18482=EDGE_CURVE('',#14490,#14490,#11808,.T.) ;
#18483=EDGE_CURVE('',#14490,#14491,#8180,.T.) ;
#18484=EDGE_CURVE('',#14491,#14491,#11809,.T.) ;
#18485=EDGE_CURVE('',#14492,#14493,#8181,.T.) ;
#18486=EDGE_CURVE('',#14492,#14494,#8182,.T.) ;
#18487=EDGE_CURVE('',#14495,#14494,#8183,.T.) ;
#18488=EDGE_CURVE('',#14495,#14493,#8184,.T.) ;
#18489=EDGE_CURVE('',#14496,#14497,#8185,.T.) ;
#18490=EDGE_CURVE('',#14496,#14498,#8186,.T.) ;
#18491=EDGE_CURVE('',#14499,#14498,#8187,.T.) ;
#18492=EDGE_CURVE('',#14499,#14497,#8188,.T.) ;
#18493=EDGE_CURVE('',#14500,#14492,#8189,.T.) ;
#18494=EDGE_CURVE('',#14498,#14500,#8190,.T.) ;
#18495=EDGE_CURVE('',#14501,#14496,#8191,.T.) ;
#18496=EDGE_CURVE('',#14494,#14501,#8192,.T.) ;
#18497=EDGE_CURVE('',#14500,#14502,#8193,.T.) ;
#18498=EDGE_CURVE('',#14493,#14502,#8194,.T.) ;
#18499=EDGE_CURVE('',#14501,#14503,#8195,.T.) ;
#18500=EDGE_CURVE('',#14497,#14503,#8196,.T.) ;
#18501=EDGE_CURVE('',#14502,#14499,#8197,.T.) ;
#18502=EDGE_CURVE('',#14503,#14495,#8198,.T.) ;
#26433=ORIENTED_EDGE('',*,*,#18482,.F.) ;
#26434=ORIENTED_EDGE('',*,*,#18483,.T.) ;
#26435=ORIENTED_EDGE('',*,*,#18484,.F.) ;
#26436=ORIENTED_EDGE('',*,*,#18483,.F.) ;
#26437=ORIENTED_EDGE('',*,*,#18485,.F.) ;
#26438=ORIENTED_EDGE('',*,*,#18486,.T.) ;
#26439=ORIENTED_EDGE('',*,*,#18487,.F.) ;
#26440=ORIENTED_EDGE('',*,*,#18488,.T.) ;
#26441=ORIENTED_EDGE('',*,*,#18489,.F.) ;
#26442=ORIENTED_EDGE('',*,*,#18490,.T.) ;
#26443=ORIENTED_EDGE('',*,*,#18491,.F.) ;
#26444=ORIENTED_EDGE('',*,*,#18492,.T.) ;
#26445=ORIENTED_EDGE('',*,*,#18486,.F.) ;
#26446=ORIENTED_EDGE('',*,*,#18493,.F.) ;
#26447=ORIENTED_EDGE('',*,*,#18494,.F.) ;
#26448=ORIENTED_EDGE('',*,*,#18490,.F.) ;
#26449=ORIENTED_EDGE('',*,*,#18495,.F.) ;
#26450=ORIENTED_EDGE('',*,*,#18496,.F.) ;
#26451=ORIENTED_EDGE('',*,*,#18482,.T.) ;
#26452=ORIENTED_EDGE('',*,*,#18497,.F.) ;
#26453=ORIENTED_EDGE('',*,*,#18493,.T.) ;
#26454=ORIENTED_EDGE('',*,*,#18485,.T.) ;
#26455=ORIENTED_EDGE('',*,*,#18498,.T.) ;
#26456=ORIENTED_EDGE('',*,*,#18499,.F.) ;
#26457=ORIENTED_EDGE('',*,*,#18495,.T.) ;
#26458=ORIENTED_EDGE('',*,*,#18489,.T.) ;
#26459=ORIENTED_EDGE('',*,*,#18500,.T.) ;
#26460=ORIENTED_EDGE('',*,*,#18497,.T.) ;
#26461=ORIENTED_EDGE('',*,*,#18501,.T.) ;
#26462=ORIENTED_EDGE('',*,*,#18491,.T.) ;
#26463=ORIENTED_EDGE('',*,*,#18494,.T.) ;
#26464=ORIENTED_EDGE('',*,*,#18487,.T.) ;
#26465=ORIENTED_EDGE('',*,*,#18496,.T.) ;
#26466=ORIENTED_EDGE('',*,*,#18499,.T.) ;
#26467=ORIENTED_EDGE('',*,*,#18502,.T.) ;
#26468=ORIENTED_EDGE('',*,*,#18488,.F.) ;
#26469=ORIENTED_EDGE('',*,*,#18502,.F.) ;
#26470=ORIENTED_EDGE('',*,*,#18500,.F.) ;
#26471=ORIENTED_EDGE('',*,*,#18492,.F.) ;
#26472=ORIENTED_EDGE('',*,*,#18501,.F.) ;
#26473=ORIENTED_EDGE('',*,*,#18498,.F.) ;
#26474=ORIENTED_EDGE('',*,*,#18484,.T.) ;
#27057=CYLINDRICAL_SURFACE('',#32246,0.5) ;
#28583=ADVANCED_FACE('',(#3848),#27057,.F.) ;
#28584=ADVANCED_FACE('',(#3849),#2323,.F.) ;
#28585=ADVANCED_FACE('',(#3850),#2324,.F.) ;
#28586=ADVANCED_FACE('',(#3851,#1404),#2325,.T.) ;
#28587=ADVANCED_FACE('',(#3852),#2326,.F.) ;
#28588=ADVANCED_FACE('',(#3853),#2327,.F.) ;
#28589=ADVANCED_FACE('',(#3854),#2328,.F.) ;
#28590=ADVANCED_FACE('',(#3855),#2329,.F.) ;
#28591=ADVANCED_FACE('',(#3856,#1405),#2330,.T.) ;
#28711=CLOSED_SHELL('',(#28583,#28584,#28585,#28586,#28587,#28588,#28589,
#28590,#28591)) ;
#32245=AXIS2_PLACEMENT_3D('',#50036,#40895,#40896) ;
#32246=AXIS2_PLACEMENT_3D('',#50037,#40897,#40898) ;
#32247=AXIS2_PLACEMENT_3D('',#50039,#40899,#40900) ;
#32248=AXIS2_PLACEMENT_3D('',#50042,#40902,#40903) ;
#32249=AXIS2_PLACEMENT_3D('',#50043,#40904,#40905) ;
#32250=AXIS2_PLACEMENT_3D('',#50052,#40910,#40911) ;
#32251=AXIS2_PLACEMENT_3D('',#50061,#40916,#40917) ;
#32252=AXIS2_PLACEMENT_3D('',#50068,#40922,#40923) ;
#32253=AXIS2_PLACEMENT_3D('',#50072,#40926,#40927) ;
#32254=AXIS2_PLACEMENT_3D('',#50076,#40930,#40931) ;
#32255=AXIS2_PLACEMENT_3D('',#50078,#40933,#40934) ;
#32256=AXIS2_PLACEMENT_3D('',#50080,#40936,#40937) ;
#40895=DIRECTION('axis',(0.,0.,1.)) ;
#40896=DIRECTION('refdir',(1.,0.,0.)) ;
#40897=DIRECTION('center_axis',(0.,1.,0.)) ;
#40898=DIRECTION('ref_axis',(1.,0.,0.)) ;
#40899=DIRECTION('center_axis',(0.,1.,0.)) ;
#40900=DIRECTION('ref_axis',(1.,0.,0.)) ;
#40901=DIRECTION('',(0.,1.,0.)) ;
#40902=DIRECTION('center_axis',(0.,-1.,0.)) ;
#40903=DIRECTION('ref_axis',(1.,0.,0.)) ;
#40904=DIRECTION('center_axis',(-0.5,0.,-0.866025403784439)) ;
#40905=DIRECTION('ref_axis',(-0.866025403784439,0.,0.5)) ;
#40906=DIRECTION('',(0.,1.,0.)) ;
#40907=DIRECTION('',(0.866025403784439,0.,-0.5)) ;
#40908=DIRECTION('',(0.,-1.,0.)) ;
#40909=DIRECTION('',(-0.866025403784439,0.,0.5)) ;
#40910=DIRECTION('center_axis',(0.5,0.,0.866025403784439)) ;
#40911=DIRECTION('ref_axis',(0.866025403784439,0.,-0.5)) ;
#40912=DIRECTION('',(0.,1.,0.)) ;
#40913=DIRECTION('',(-0.866025403784439,0.,0.5)) ;
#40914=DIRECTION('',(0.,-1.,0.)) ;
#40915=DIRECTION('',(0.866025403784439,0.,-0.5)) ;
#40916=DIRECTION('center_axis',(0.,-1.,0.)) ;
#40917=DIRECTION('ref_axis',(-1.,0.,0.)) ;
#40918=DIRECTION('',(0.866025403784439,0.,0.5)) ;
#40919=DIRECTION('',(0.,0.,1.)) ;
#40920=DIRECTION('',(-0.866025403784439,0.,-0.5)) ;
#40921=DIRECTION('',(0.,0.,-1.)) ;
#40922=DIRECTION('center_axis',(0.5,0.,-0.866025403784439)) ;
#40923=DIRECTION('ref_axis',(-0.866025403784439,0.,-0.5)) ;
#40924=DIRECTION('',(0.,1.,0.)) ;
#40925=DIRECTION('',(-0.866025403784439,0.,-0.5)) ;
#40926=DIRECTION('center_axis',(-0.5,0.,0.866025403784439)) ;
#40927=DIRECTION('ref_axis',(0.866025403784439,0.,0.5)) ;
#40928=DIRECTION('',(0.,1.,0.)) ;
#40929=DIRECTION('',(0.866025403784439,0.,0.5)) ;
#40930=DIRECTION('center_axis',(1.,0.,0.)) ;
#40931=DIRECTION('ref_axis',(0.,0.,-1.)) ;
#40932=DIRECTION('',(0.,0.,-1.)) ;
#40933=DIRECTION('center_axis',(-1.,0.,0.)) ;
#40934=DIRECTION('ref_axis',(0.,0.,1.)) ;
#40935=DIRECTION('',(0.,0.,1.)) ;
#40936=DIRECTION('center_axis',(0.,1.,0.)) ;
#40937=DIRECTION('ref_axis',(1.,0.,0.)) ;
#50036=CARTESIAN_POINT('',(0.,0.,0.)) ;
#50037=CARTESIAN_POINT('Origin',(-53.,20.,92.)) ;
#50038=CARTESIAN_POINT('',(-53.5,19.7,92.)) ;
#50039=CARTESIAN_POINT('Origin',(-53.,19.7,92.)) ;
#50040=CARTESIAN_POINT('',(-53.5,20.3,92.)) ;
#50041=CARTESIAN_POINT('',(-53.5,20.,92.)) ;
#50042=CARTESIAN_POINT('Origin',(-53.,20.3,92.)) ;
#50043=CARTESIAN_POINT('Origin',(-52.575,20.,92.7361215932168)) ;
#50044=CARTESIAN_POINT('',(-53.,19.7,92.9814954576224)) ;
#50045=CARTESIAN_POINT('',(-53.,20.3,92.9814954576224)) ;
#50046=CARTESIAN_POINT('',(-53.,20.,92.9814954576224)) ;
#50047=CARTESIAN_POINT('',(-52.15,19.7,92.4907477288112)) ;
#50048=CARTESIAN_POINT('',(-52.575,19.7,92.7361215932168)) ;
#50049=CARTESIAN_POINT('',(-52.15,20.3,92.4907477288112)) ;
#50050=CARTESIAN_POINT('',(-52.15,20.,92.4907477288112)) ;
#50051=CARTESIAN_POINT('',(-52.575,20.3,92.7361215932168)) ;
#50052=CARTESIAN_POINT('Origin',(-53.425,20.,91.2638784067832)) ;
#50053=CARTESIAN_POINT('',(-53.,19.7,91.0185045423776)) ;
#50054=CARTESIAN_POINT('',(-53.,20.3,91.0185045423776)) ;
#50055=CARTESIAN_POINT('',(-53.,20.,91.0185045423776)) ;
#50056=CARTESIAN_POINT('',(-53.85,19.7,91.5092522711888)) ;
#50057=CARTESIAN_POINT('',(-53.425,19.7,91.2638784067832)) ;
#50058=CARTESIAN_POINT('',(-53.85,20.3,91.5092522711888)) ;
#50059=CARTESIAN_POINT('',(-53.85,20.,91.5092522711888)) ;
#50060=CARTESIAN_POINT('',(-53.425,20.3,91.2638784067832)) ;
#50061=CARTESIAN_POINT('Origin',(-53.,19.7,92.)) ;
#50062=CARTESIAN_POINT('',(-53.85,19.7,92.4907477288112)) ;
#50063=CARTESIAN_POINT('',(-53.425,19.7,92.7361215932168)) ;
#50064=CARTESIAN_POINT('',(-53.85,19.7,92.)) ;
#50065=CARTESIAN_POINT('',(-52.15,19.7,91.5092522711888)) ;
#50066=CARTESIAN_POINT('',(-52.575,19.7,91.2638784067832)) ;
#50067=CARTESIAN_POINT('',(-52.15,19.7,92.)) ;
#50068=CARTESIAN_POINT('Origin',(-53.425,20.,92.7361215932168)) ;
#50069=CARTESIAN_POINT('',(-53.85,20.3,92.4907477288112)) ;
#50070=CARTESIAN_POINT('',(-53.85,20.,92.4907477288112)) ;
#50071=CARTESIAN_POINT('',(-53.425,20.3,92.7361215932168)) ;
#50072=CARTESIAN_POINT('Origin',(-52.575,20.,91.2638784067832)) ;
#50073=CARTESIAN_POINT('',(-52.15,20.3,91.5092522711888)) ;
#50074=CARTESIAN_POINT('',(-52.15,20.,91.5092522711888)) ;
#50075=CARTESIAN_POINT('',(-52.575,20.3,91.2638784067832)) ;
#50076=CARTESIAN_POINT('Origin',(-53.85,20.,92.)) ;
#50077=CARTESIAN_POINT('',(-53.85,20.3,92.)) ;
#50078=CARTESIAN_POINT('Origin',(-52.15,20.,92.)) ;
#50079=CARTESIAN_POINT('',(-52.15,20.3,92.)) ;
#50080=CARTESIAN_POINT('Origin',(-53.,20.3,92.)) ;
#50383=UNCERTAINTY_MEASURE_WITH_UNIT(LENGTH_MEASURE(0.001),#50441,
'DISTANCE_ACCURACY_VALUE',
'Maximum model space distance between geometric entities at asserted c
onnectivities') ;
#50387=UNCERTAINTY_MEASURE_WITH_UNIT(LENGTH_MEASURE(0.001),#50441,
'DISTANCE_ACCURACY_VALUE',
'Maximum model space distance between geometric entities at asserted c
onnectivities') ;
#50436=(
GEOMETRIC_REPRESENTATION_CONTEXT(3)
GLOBAL_UNCERTAINTY_ASSIGNED_CONTEXT((#50383))
GLOBAL_UNIT_ASSIGNED_CONTEXT((#50441,#50443,#50444))
REPRESENTATION_CONTEXT('','3D')
) ;
#50440=(
GEOMETRIC_REPRESENTATION_CONTEXT(3)
GLOBAL_UNCERTAINTY_ASSIGNED_CONTEXT((#50387))
GLOBAL_UNIT_ASSIGNED_CONTEXT((#50441,#50443,#50444))
REPRESENTATION_CONTEXT('','3D')
) ;
#50441=(
LENGTH_UNIT()
NAMED_UNIT(*)
SI_UNIT(.CENTI.,.METRE.)
) ;
#50443=(
NAMED_UNIT(*)
PLANE_ANGLE_UNIT()
SI_UNIT($,.RADIAN.)
) ;
#50444=(
NAMED_UNIT(*)
SI_UNIT($,.STERADIAN.)
SOLID_ANGLE_UNIT()
) ;
#50493=SHAPE_DEFINITION_REPRESENTATION(#50589,#50667) ;
#50589=PRODUCT_DEFINITION_SHAPE('',$,#50720) ;
#50667=SHAPE_REPRESENTATION('',(#32245),#50436) ;
#50671=PRODUCT_DEFINITION_CONTEXT('part definition',#50829,'design') ;
#50720=PRODUCT_DEFINITION('LEVER_PIVOT_NUT_M10',
'LEVER_PIVOT_NUT_M10',#50772,#50671) ;
#50772=PRODUCT_DEFINITION_FORMATION('',$,#50879) ;
#50829=APPLICATION_CONTEXT(
'Core Data for Automotive Mechanical Design Process') ;
#50830=PRODUCT_CONTEXT('part definition',#50829,'mechanical') ;
#50879=PRODUCT('LEVER_PIVOT_NUT_M10','LEVER_PIVOT_NUT_M10',$,(#50830)) ;
#50883=PRESENTATION_STYLE_ASSIGNMENT((#50890)) ;
#50890=SURFACE_STYLE_USAGE(.BOTH.,#50897) ;
#50897=SURFACE_SIDE_STYLE('',(#50904)) ;
#50904=SURFACE_STYLE_FILL_AREA(#50911) ;
#50911=FILL_AREA_STYLE('Steel - Satin',(#50918)) ;
#50918=FILL_AREA_STYLE_COLOUR('Steel - Satin',#50925) ;
#50925=COLOUR_RGB('Steel - Satin', 0.31764706, 0.68627451, 0.89019608) ;
ENDSEC;
END-ISO-10303-21;
